ISO-10303-21;
HEADER;
/* Generated by software containing ST-Developer
 * from STEP Tools, Inc. (www.steptools.com) 
 */

FILE_DESCRIPTION(
/* description */ ('Double-row support with tensioned shaft'),
/* implementation_level */ '2;1');

FILE_NAME(
/* name */ 'Flat Washer - M8.step',
/* time_stamp */ '2026-10-27T10:50:35-07:00',
/* author */ (''),
/* organization */ (''),
/* preprocessor_version */ 'ST-DEVELOPER v20.2',
/* originating_system */ 'Autodesk Translation Framework v15.17.0.0',
/* authorisation */ '');

FILE_SCHEMA (('AUTOMOTIVE_DESIGN { 1 0 10303 214 3 1 1 }'));
ENDSEC;

DATA;
#10=MECHANICAL_DESIGN_GEOMETRIC_PRESENTATION_REPRESENTATION('',(#502),#11559);
#437=SHAPE_REPRESENTATION_RELATIONSHIP('SRR','None',#11746,#469);
#469=ADVANCED_BREP_SHAPE_REPRESENTATION('',(#532),#11548);
#502=STYLED_ITEM('',(#11974),#532);
#532=MANIFOLD_SOLID_BREP('Body1',#6350);
#649=FACE_BOUND('',#1622,.T.);
#650=FACE_BOUND('',#1624,.T.);
#850=PLANE('',#7140);
#851=PLANE('',#7141);
#1168=FACE_OUTER_BOUND('',#1619,.T.);
#1169=FACE_OUTER_BOUND('',#1620,.T.);
#1170=FACE_OUTER_BOUND('',#1621,.T.);
#1171=FACE_OUTER_BOUND('',#1623,.T.);
#1619=EDGE_LOOP('',(#5494,#5495,#5496,#5497));
#1620=EDGE_LOOP('',(#5498,#5499,#5500,#5501));
#1621=EDGE_LOOP('',(#5502));
#1622=EDGE_LOOP('',(#5503));
#1623=EDGE_LOOP('',(#5504));
#1624=EDGE_LOOP('',(#5505));
#2158=LINE('',#10899,#2705);
#2159=LINE('',#10905,#2706);
#2705=VECTOR('',#8633,0.42);
#2706=VECTOR('',#8640,0.8);
#2976=CIRCLE('',#7135,0.42);
#2977=CIRCLE('',#7136,0.42);
#2978=CIRCLE('',#7138,0.8);
#2979=CIRCLE('',#7139,0.8);
#3419=VERTEX_POINT('',#10896);
#3420=VERTEX_POINT('',#10898);
#3421=VERTEX_POINT('',#10902);
#3422=VERTEX_POINT('',#10904);
#4132=EDGE_CURVE('',#3419,#3419,#2976,.T.);
#4133=EDGE_CURVE('',#3419,#3420,#2158,.T.);
#4134=EDGE_CURVE('',#3420,#3420,#2977,.T.);
#4135=EDGE_CURVE('',#3421,#3421,#2978,.T.);
#4136=EDGE_CURVE('',#3421,#3422,#2159,.T.);
#4137=EDGE_CURVE('',#3422,#3422,#2979,.T.);
#5494=ORIENTED_EDGE('',*,*,#4132,.F.);
#5495=ORIENTED_EDGE('',*,*,#4133,.T.);
#5496=ORIENTED_EDGE('',*,*,#4134,.T.);
#5497=ORIENTED_EDGE('',*,*,#4133,.F.);
#5498=ORIENTED_EDGE('',*,*,#4135,.F.);
#5499=ORIENTED_EDGE('',*,*,#4136,.T.);
#5500=ORIENTED_EDGE('',*,*,#4137,.T.);
#5501=ORIENTED_EDGE('',*,*,#4136,.F.);
#5502=ORIENTED_EDGE('',*,*,#4135,.T.);
#5503=ORIENTED_EDGE('',*,*,#4132,.T.);
#5504=ORIENTED_EDGE('',*,*,#4137,.F.);
#5505=ORIENTED_EDGE('',*,*,#4134,.F.);
#5958=CYLINDRICAL_SURFACE('',#7134,0.42);
#5959=CYLINDRICAL_SURFACE('',#7137,0.8);
#6231=ADVANCED_FACE('',(#1168),#5958,.F.);
#6232=ADVANCED_FACE('',(#1169),#5959,.T.);
#6233=ADVANCED_FACE('',(#1170,#649),#850,.T.);
#6234=ADVANCED_FACE('',(#1171,#650),#851,.F.);
#6350=CLOSED_SHELL('',(#6231,#6232,#6233,#6234));
#7133=AXIS2_PLACEMENT_3D('',#10894,#8627,#8628);
#7134=AXIS2_PLACEMENT_3D('',#10895,#8629,#8630);
#7135=AXIS2_PLACEMENT_3D('',#10897,#8631,#8632);
#7136=AXIS2_PLACEMENT_3D('',#10900,#8634,#8635);
#7137=AXIS2_PLACEMENT_3D('',#10901,#8636,#8637);
#7138=AXIS2_PLACEMENT_3D('',#10903,#8638,#8639);
#7139=AXIS2_PLACEMENT_3D('',#10906,#8641,#8642);
#7140=AXIS2_PLACEMENT_3D('',#10907,#8643,#8644);
#7141=AXIS2_PLACEMENT_3D('',#10908,#8645,#8646);
#8627=DIRECTION('axis',(0.,0.,1.));
#8628=DIRECTION('refdir',(1.,0.,0.));
#8629=DIRECTION('center_axis',(0.,1.,0.));
#8630=DIRECTION('ref_axis',(1.,0.,0.));
#8631=DIRECTION('center_axis',(0.,-1.,0.));
#8632=DIRECTION('ref_axis',(1.,0.,0.));
#8633=DIRECTION('',(0.,-1.,0.));
#8634=DIRECTION('center_axis',(0.,-1.,0.));
#8635=DIRECTION('ref_axis',(1.,0.,0.));
#8636=DIRECTION('center_axis',(0.,1.,0.));
#8637=DIRECTION('ref_axis',(1.,0.,0.));
#8638=DIRECTION('center_axis',(0.,1.,0.));
#8639=DIRECTION('ref_axis',(1.,0.,0.));
#8640=DIRECTION('',(0.,-1.,0.));
#8641=DIRECTION('center_axis',(0.,1.,0.));
#8642=DIRECTION('ref_axis',(1.,0.,0.));
#8643=DIRECTION('center_axis',(0.,1.,0.));
#8644=DIRECTION('ref_axis',(1.,0.,0.));
#8645=DIRECTION('center_axis',(0.,1.,0.));
#8646=DIRECTION('ref_axis',(1.,0.,0.));
#10894=CARTESIAN_POINT('',(0.,0.,0.));
#10895=CARTESIAN_POINT('Origin',(0.,0.,0.));
#10896=CARTESIAN_POINT('',(-0.42,0.16,5.14351655641888E-17));
#10897=CARTESIAN_POINT('Origin',(0.,0.16,0.));
#10898=CARTESIAN_POINT('',(-0.42,0.,5.14351655641888E-17));
#10899=CARTESIAN_POINT('',(-0.42,0.,5.14351655641888E-17));
#10900=CARTESIAN_POINT('Origin',(0.,0.,0.));
#10901=CARTESIAN_POINT('Origin',(0.,0.,0.));
#10902=CARTESIAN_POINT('',(-0.8,0.16,9.79717439317883E-17));
#10903=CARTESIAN_POINT('Origin',(0.,0.16,0.));
#10904=CARTESIAN_POINT('',(-0.8,0.,9.79717439317883E-17));
#10905=CARTESIAN_POINT('',(-0.8,0.,9.79717439317883E-17));
#10906=CARTESIAN_POINT('Origin',(0.,0.,0.));
#10907=CARTESIAN_POINT('Origin',(0.,0.16,0.));
#10908=CARTESIAN_POINT('Origin',(0.,0.,0.));
#11511=UNCERTAINTY_MEASURE_WITH_UNIT(LENGTH_MEASURE(0.001),#11560,
'DISTANCE_ACCURACY_VALUE',
'Maximum model space distance between geometric entities at asserted c
onnectivities');
#11522=UNCERTAINTY_MEASURE_WITH_UNIT(LENGTH_MEASURE(0.001),#11560,
'DISTANCE_ACCURACY_VALUE',
'Maximum model space distance between geometric entities at asserted c
onnectivities');
#11548=(
GEOMETRIC_REPRESENTATION_CONTEXT(3)
GLOBAL_UNCERTAINTY_ASSIGNED_CONTEXT((#11511))
GLOBAL_UNIT_ASSIGNED_CONTEXT((#11560,#11562,#11563))
REPRESENTATION_CONTEXT('','3D')
);
#11559=(
GEOMETRIC_REPRESENTATION_CONTEXT(3)
GLOBAL_UNCERTAINTY_ASSIGNED_CONTEXT((#11522))
GLOBAL_UNIT_ASSIGNED_CONTEXT((#11560,#11562,#11563))
REPRESENTATION_CONTEXT('','3D')
);
#11560=(
LENGTH_UNIT()
NAMED_UNIT(*)
SI_UNIT(.CENTI.,.METRE.)
);
#11562=(
NAMED_UNIT(*)
PLANE_ANGLE_UNIT()
SI_UNIT($,.RADIAN.)
);
#11563=(
NAMED_UNIT(*)
SI_UNIT($,.STERADIAN.)
SOLID_ANGLE_UNIT()
);
#11589=SHAPE_DEFINITION_REPRESENTATION(#11627,#11746);
#11627=PRODUCT_DEFINITION_SHAPE('',$,#11783);
#11746=SHAPE_REPRESENTATION('',(#7133),#11548);
#11757=PRODUCT_DEFINITION_CONTEXT('part definition',#11867,'design');
#11783=PRODUCT_DEFINITION('Flat Washer - M8','Flat Washer - M8',#11819,
#11757);
#11819=PRODUCT_DEFINITION_FORMATION('',$,#11894);
#11867=APPLICATION_CONTEXT(
'Core Data for Automotive Mechanical Design Process');
#11868=PRODUCT_CONTEXT('part definition',#11867,'mechanical');
#11894=PRODUCT('Flat Washer - M8','Flat Washer - M8','Flat Washer - M8',
(#11868));
#11968=COLOUR_RGB('Black',0.12,0.14,0.17);
#11969=FILL_AREA_STYLE_COLOUR('',#11968);
#11970=FILL_AREA_STYLE('',(#11969));
#11971=SURFACE_STYLE_FILL_AREA(#11970);
#11972=SURFACE_SIDE_STYLE('',(#11971));
#11973=SURFACE_STYLE_USAGE(.BOTH.,#11972);
#11974=PRESENTATION_STYLE_ASSIGNMENT((#11973));
ENDSEC;
END-ISO-10303-21;
